ISO-10303-21;
HEADER;
/* Generated by software containing ST-Developer
 * from STEP Tools, Inc. (www.steptools.com) 
 */

FILE_DESCRIPTION(
/* description */ ('PAT-072'),
/* implementation_level */ '2;1');

FILE_NAME(
/* name */ 'Metering plug (1).step',
/* time_stamp */ '2026-10-29T20:11:56-07:00',
/* author */ (''),
/* organization */ (''),
/* preprocessor_version */ 'ST-DEVELOPER v20.2',
/* originating_system */ 'Autodesk Translation Framework v15.17.0.0',
/* authorisation */ '');

FILE_SCHEMA (('AUTOMOTIVE_DESIGN { 1 0 10303 214 3 1 1 }'));
ENDSEC;

DATA;
#10=MECHANICAL_DESIGN_GEOMETRIC_PRESENTATION_REPRESENTATION('',(#340),#11432);
#268=SHAPE_REPRESENTATION_RELATIONSHIP('SRR','None',#11572,#304);
#304=ADVANCED_BREP_SHAPE_REPRESENTATION('',(#376),#11403);
#340=STYLED_ITEM('',(#11812),#376);
#376=MANIFOLD_SOLID_BREP('Body1',#6075);
#468=FACE_BOUND('',#1351,.T.);
#469=FACE_BOUND('',#1355,.T.);
#631=PLANE('',#6734);
#632=PLANE('',#6739);
#633=PLANE('',#6740);
#634=PLANE('',#6746);
#912=FACE_OUTER_BOUND('',#1350,.T.);
#913=FACE_OUTER_BOUND('',#1352,.T.);
#914=FACE_OUTER_BOUND('',#1353,.T.);
#915=FACE_OUTER_BOUND('',#1354,.T.);
#916=FACE_OUTER_BOUND('',#1356,.T.);
#917=FACE_OUTER_BOUND('',#1357,.T.);
#918=FACE_OUTER_BOUND('',#1358,.T.);
#1350=EDGE_LOOP('',(#4552));
#1351=EDGE_LOOP('',(#4553));
#1352=EDGE_LOOP('',(#4554,#4555,#4556,#4557));
#1353=EDGE_LOOP('',(#4558));
#1354=EDGE_LOOP('',(#4559));
#1355=EDGE_LOOP('',(#4560));
#1356=EDGE_LOOP('',(#4561,#4562,#4563,#4564));
#1357=EDGE_LOOP('',(#4565,#4566,#4567,#4568));
#1358=EDGE_LOOP('',(#4569));
#1819=LINE('',#10065,#2238);
#1820=LINE('',#10073,#2239);
#1821=LINE('',#10076,#2240);
#2238=VECTOR('',#7844,0.6);
#2239=VECTOR('',#7855,0.3);
#2240=VECTOR('',#7858,0.1);
#2645=CIRCLE('',#6735,0.6);
#2646=CIRCLE('',#6736,0.3);
#2647=CIRCLE('',#6738,0.6);
#2648=CIRCLE('',#6741,0.3);
#2649=CIRCLE('',#6742,0.1);
#2650=CIRCLE('',#6745,0.1);
#2994=VERTEX_POINT('',#10058);
#2995=VERTEX_POINT('',#10060);
#2996=VERTEX_POINT('',#10063);
#2997=VERTEX_POINT('',#10068);
#2998=VERTEX_POINT('',#10070);
#2999=VERTEX_POINT('',#10075);
#3565=EDGE_CURVE('',#2994,#2994,#2645,.T.);
#3566=EDGE_CURVE('',#2995,#2995,#2646,.T.);
#3567=EDGE_CURVE('',#2996,#2996,#2647,.T.);
#3568=EDGE_CURVE('',#2996,#2994,#1819,.T.);
#3569=EDGE_CURVE('',#2997,#2997,#2648,.T.);
#3570=EDGE_CURVE('',#2998,#2998,#2649,.T.);
#3571=EDGE_CURVE('',#2995,#2997,#1820,.T.);
#3572=EDGE_CURVE('',#2998,#2999,#1821,.T.);
#3573=EDGE_CURVE('',#2999,#2999,#2650,.T.);
#4552=ORIENTED_EDGE('',*,*,#3565,.F.);
#4553=ORIENTED_EDGE('',*,*,#3566,.T.);
#4554=ORIENTED_EDGE('',*,*,#3567,.F.);
#4555=ORIENTED_EDGE('',*,*,#3568,.T.);
#4556=ORIENTED_EDGE('',*,*,#3565,.T.);
#4557=ORIENTED_EDGE('',*,*,#3568,.F.);
#4558=ORIENTED_EDGE('',*,*,#3567,.T.);
#4559=ORIENTED_EDGE('',*,*,#3569,.F.);
#4560=ORIENTED_EDGE('',*,*,#3570,.T.);
#4561=ORIENTED_EDGE('',*,*,#3566,.F.);
#4562=ORIENTED_EDGE('',*,*,#3571,.T.);
#4563=ORIENTED_EDGE('',*,*,#3569,.T.);
#4564=ORIENTED_EDGE('',*,*,#3571,.F.);
#4565=ORIENTED_EDGE('',*,*,#3570,.F.);
#4566=ORIENTED_EDGE('',*,*,#3572,.T.);
#4567=ORIENTED_EDGE('',*,*,#3573,.T.);
#4568=ORIENTED_EDGE('',*,*,#3572,.F.);
#4569=ORIENTED_EDGE('',*,*,#3573,.F.);
#5613=CYLINDRICAL_SURFACE('',#6737,0.6);
#5614=CYLINDRICAL_SURFACE('',#6743,0.3);
#5615=CYLINDRICAL_SURFACE('',#6744,0.1);
#5811=ADVANCED_FACE('',(#912,#468),#631,.F.);
#5812=ADVANCED_FACE('',(#913),#5613,.T.);
#5813=ADVANCED_FACE('',(#914),#632,.T.);
#5814=ADVANCED_FACE('',(#915,#469),#633,.F.);
#5815=ADVANCED_FACE('',(#916),#5614,.T.);
#5816=ADVANCED_FACE('',(#917),#5615,.T.);
#5817=ADVANCED_FACE('',(#918),#634,.F.);
#6075=CLOSED_SHELL('',(#5811,#5812,#5813,#5814,#5815,#5816,#5817));
#6733=AXIS2_PLACEMENT_3D('',#10056,#7832,#7833);
#6734=AXIS2_PLACEMENT_3D('',#10057,#7834,#7835);
#6735=AXIS2_PLACEMENT_3D('',#10059,#7836,#7837);
#6736=AXIS2_PLACEMENT_3D('',#10061,#7838,#7839);
#6737=AXIS2_PLACEMENT_3D('',#10062,#7840,#7841);
#6738=AXIS2_PLACEMENT_3D('',#10064,#7842,#7843);
#6739=AXIS2_PLACEMENT_3D('',#10066,#7845,#7846);
#6740=AXIS2_PLACEMENT_3D('',#10067,#7847,#7848);
#6741=AXIS2_PLACEMENT_3D('',#10069,#7849,#7850);
#6742=AXIS2_PLACEMENT_3D('',#10071,#7851,#7852);
#6743=AXIS2_PLACEMENT_3D('',#10072,#7853,#7854);
#6744=AXIS2_PLACEMENT_3D('',#10074,#7856,#7857);
#6745=AXIS2_PLACEMENT_3D('',#10077,#7859,#7860);
#6746=AXIS2_PLACEMENT_3D('',#10078,#7861,#7862);
#7832=DIRECTION('axis',(0.,0.,1.));
#7833=DIRECTION('refdir',(1.,0.,0.));
#7834=DIRECTION('center_axis',(0.,0.,1.));
#7835=DIRECTION('ref_axis',(1.,0.,0.));
#7836=DIRECTION('center_axis',(0.,0.,1.));
#7837=DIRECTION('ref_axis',(1.,0.,0.));
#7838=DIRECTION('center_axis',(0.,0.,1.));
#7839=DIRECTION('ref_axis',(1.,0.,0.));
#7840=DIRECTION('center_axis',(0.,0.,1.));
#7841=DIRECTION('ref_axis',(1.,0.,0.));
#7842=DIRECTION('center_axis',(0.,0.,1.));
#7843=DIRECTION('ref_axis',(1.,0.,0.));
#7844=DIRECTION('',(0.,0.,-1.));
#7845=DIRECTION('center_axis',(0.,0.,1.));
#7846=DIRECTION('ref_axis',(1.,0.,0.));
#7847=DIRECTION('center_axis',(0.,0.,1.));
#7848=DIRECTION('ref_axis',(1.,0.,0.));
#7849=DIRECTION('center_axis',(0.,0.,1.));
#7850=DIRECTION('ref_axis',(1.,0.,0.));
#7851=DIRECTION('center_axis',(0.,0.,1.));
#7852=DIRECTION('ref_axis',(1.,0.,0.));
#7853=DIRECTION('center_axis',(0.,0.,1.));
#7854=DIRECTION('ref_axis',(1.,0.,0.));
#7855=DIRECTION('',(0.,0.,-1.));
#7856=DIRECTION('center_axis',(0.,0.,1.));
#7857=DIRECTION('ref_axis',(1.,0.,0.));
#7858=DIRECTION('',(0.,0.,-1.));
#7859=DIRECTION('center_axis',(0.,0.,1.));
#7860=DIRECTION('ref_axis',(1.,0.,0.));
#7861=DIRECTION('center_axis',(0.,0.,1.));
#7862=DIRECTION('ref_axis',(1.,0.,0.));
#10056=CARTESIAN_POINT('',(0.,0.,0.));
#10057=CARTESIAN_POINT('Origin',(-1.25,1.5,6.1));
#10058=CARTESIAN_POINT('',(-1.85,1.5,6.1));
#10059=CARTESIAN_POINT('Origin',(-1.25,1.5,6.1));
#10060=CARTESIAN_POINT('',(-1.55,1.5,6.1));
#10061=CARTESIAN_POINT('Origin',(-1.25,1.5,6.1));
#10062=CARTESIAN_POINT('Origin',(-1.25,1.5,6.1));
#10063=CARTESIAN_POINT('',(-1.85,1.5,6.5));
#10064=CARTESIAN_POINT('Origin',(-1.25,1.5,6.5));
#10065=CARTESIAN_POINT('',(-1.85,1.5,6.1));
#10066=CARTESIAN_POINT('Origin',(-1.25,1.5,6.5));
#10067=CARTESIAN_POINT('Origin',(-1.25,1.5,4.8));
#10068=CARTESIAN_POINT('',(-1.55,1.5,4.8));
#10069=CARTESIAN_POINT('Origin',(-1.25,1.5,4.8));
#10070=CARTESIAN_POINT('',(-1.35,1.5,4.8));
#10071=CARTESIAN_POINT('Origin',(-1.25,1.5,4.8));
#10072=CARTESIAN_POINT('Origin',(-1.25,1.5,4.8));
#10073=CARTESIAN_POINT('',(-1.55,1.5,4.8));
#10074=CARTESIAN_POINT('Origin',(-1.25,1.5,4.1));
#10075=CARTESIAN_POINT('',(-1.35,1.5,4.1));
#10076=CARTESIAN_POINT('',(-1.35,1.5,4.1));
#10077=CARTESIAN_POINT('Origin',(-1.25,1.5,4.1));
#10078=CARTESIAN_POINT('Origin',(-1.25,1.5,4.1));
#11364=UNCERTAINTY_MEASURE_WITH_UNIT(LENGTH_MEASURE(0.001),#11433,
'DISTANCE_ACCURACY_VALUE',
'Maximum model space distance between geometric entities at asserted c
onnectivities');
#11393=UNCERTAINTY_MEASURE_WITH_UNIT(LENGTH_MEASURE(0.001),#11433,
'DISTANCE_ACCURACY_VALUE',
'Maximum model space distance between geometric entities at asserted c
onnectivities');
#11403=(
GEOMETRIC_REPRESENTATION_CONTEXT(3)
GLOBAL_UNCERTAINTY_ASSIGNED_CONTEXT((#11364))
GLOBAL_UNIT_ASSIGNED_CONTEXT((#11433,#11435,#11436))
REPRESENTATION_CONTEXT('','3D')
);
#11432=(
GEOMETRIC_REPRESENTATION_CONTEXT(3)
GLOBAL_UNCERTAINTY_ASSIGNED_CONTEXT((#11393))
GLOBAL_UNIT_ASSIGNED_CONTEXT((#11433,#11435,#11436))
REPRESENTATION_CONTEXT('','3D')
);
#11433=(
LENGTH_UNIT()
NAMED_UNIT(*)
SI_UNIT(.CENTI.,.METRE.)
);
#11435=(
NAMED_UNIT(*)
PLANE_ANGLE_UNIT()
SI_UNIT($,.RADIAN.)
);
#11436=(
NAMED_UNIT(*)
SI_UNIT($,.STERADIAN.)
SOLID_ANGLE_UNIT()
);
#11446=SHAPE_DEFINITION_REPRESENTATION(#11484,#11572);
#11484=PRODUCT_DEFINITION_SHAPE('',$,#11611);
#11572=SHAPE_REPRESENTATION('',(#6733),#11403);
#11601=PRODUCT_DEFINITION_CONTEXT('part definition',#11717,'design');
#11611=PRODUCT_DEFINITION('Metering plug (1)',
'Metering plug (1)',#11649,#11601);
#11649=PRODUCT_DEFINITION_FORMATION('',$,#11728);
#11717=APPLICATION_CONTEXT(
'Core Data for Automotive Mechanical Design Process');
#11718=PRODUCT_CONTEXT('part definition',#11717,'mechanical');
#11728=PRODUCT('Metering plug (1)','Metering plug (1)',
'Metering plug (1)',(#11718));
#11806=COLOUR_RGB('Sky Blue',0.24,0.69,0.87);
#11807=FILL_AREA_STYLE_COLOUR('',#11806);
#11808=FILL_AREA_STYLE('',(#11807));
#11809=SURFACE_STYLE_FILL_AREA(#11808);
#11810=SURFACE_SIDE_STYLE('',(#11809));
#11811=SURFACE_STYLE_USAGE(.BOTH.,#11810);
#11812=PRESENTATION_STYLE_ASSIGNMENT((#11811));
ENDSEC;
END-ISO-10303-21;
